ISO-10303-21;
HEADER;
FILE_DESCRIPTION (('STEP AP214'),
    '1' );
FILE_NAME ('circlip for shafts normal_din_Circlip DIN 471 - 22 x 1.2.step',
    '2026-09-28T15:49:00',
    ( '' ),
    ( '' ),
    'SwSTEP 2.0',
    'SolidWorks 2026',
    '' );
FILE_SCHEMA (( 'AUTOMOTIVE_DESIGN' ));
ENDSEC;

DATA;
#13=CARTESIAN_POINT ( 'NONE',  ( -12.55910585664919132, 0.7408941433508802188, -1.200000000000006617 ) ) ;
#113=CARTESIAN_POINT ( 'NONE',  ( 3.983177536951269193, -13.66651769228263724, -1.200000000000006617 ) ) ;
#119=DIRECTION ( 'NONE',  ( 1.000000000000000000, 0.000000000000000000, 0.000000000000000000 ) ) ;
#135=LINE ( 'NONE', #21918, #20318 ) ;
#209=VERTEX_POINT ( 'NONE', #26030 ) ;
#265=CARTESIAN_POINT ( 'NONE',  ( -2.600000000000004530, -12.74999999999999822, -1.386669559958809814E-29 ) ) ;
#307=ORIENTED_EDGE ( 'NONE', *, *, #12809, .F. ) ;
#382=ORIENTED_EDGE ( 'NONE', *, *, #11261, .F. ) ;
#413=DIRECTION ( 'NONE',  ( 1.000000000000000000, 0.000000000000000000, 0.000000000000000000 ) ) ;
#487=ADVANCED_BREP_SHAPE_REPRESENTATION ( '', ( #34958, #21307 ), #24211 ) ;
#502=CARTESIAN_POINT ( 'NONE',  ( 0.6000000000000035305, -12.74999999999999822, -1.386669559958809814E-29 ) ) ;
#539=ORIENTED_EDGE ( 'NONE', *, *, #35544, .F. ) ;
#550=COLOUR_RGB ( '', 0.72549020, 0.75294118, 0.79215686) ;
#571=FILL_AREA_STYLE_COLOUR ( '', #26846 ) ;
#580=VERTEX_POINT ( 'NONE', #778 ) ;
#632=CARTESIAN_POINT ( 'NONE',  ( 10.50000000000000178, -7.127471650355167704E-32, -1.232595164407830946E-29 ) ) ;
#778=CARTESIAN_POINT ( 'NONE',  ( -5.639656061357301020, -10.48075544252181857, 0.000000000000000000 ) ) ;
#780=CARTESIAN_POINT ( 'NONE',  ( 3.413765605486549060, -14.29811891091956078, -1.200000000000006617 ) ) ;
#787=EDGE_LOOP ( 'NONE', ( #1518, #3931, #9120, #16817 ) ) ;
#980=ORIENTED_EDGE ( 'NONE', *, *, #19432, .T. ) ;
#990=EDGE_LOOP ( 'NONE', ( #27082, #22848, #13873, #14916 ) ) ;
#1028=CARTESIAN_POINT ( 'NONE',  ( 1.600000000000004086, -12.74999999999999822, -1.200000000000006617 ) ) ;
#1029=DIRECTION ( 'NONE',  ( 1.000000000000000000, 0.000000000000000000, 0.000000000000000000 ) ) ;
#1053=PLANE ( 'NONE',  #11134 ) ;
#1152=PRODUCT_DEFINITION_FORMATION_WITH_SPECIFIED_SOURCE ( 'ANY', '', #28786, .NOT_KNOWN. ) ;
#1226=CARTESIAN_POINT ( 'NONE',  ( -0.2142857142857362840, -10.49781318335649161, -1.200000000000006617 ) ) ;
#1335=ADVANCED_FACE ( 'NONE', ( #18007 ), #20877, .T. ) ;
#1404=LINE ( 'NONE', #12027, #34902 ) ;
#1417=ORIENTED_EDGE ( 'NONE', *, *, #6170, .T. ) ;
#1433=DIRECTION ( 'NONE',  ( -1.000000000000000000, 0.000000000000000000, 1.691777834109591283E-31 ) ) ;
#1518=ORIENTED_EDGE ( 'NONE', *, *, #22975, .F. ) ;
#1545=DIRECTION ( 'NONE',  ( -1.783119874454246424E-31, -1.187911941725854497E-31, 1.000000000000000000 ) ) ;
#1609=CARTESIAN_POINT ( 'NONE',  ( 0.000000000000000000, 0.000000000000000000, 0.000000000000000000 ) ) ;
#1610=CYLINDRICAL_SURFACE ( 'NONE', #19412, 12.55910585664918422 ) ;
#1711=CIRCLE ( 'NONE', #21825, 2.799122904894268071 ) ;
#1827=EDGE_LOOP ( 'NONE', ( #8246, #13023 ) ) ;
#1832=AXIS2_PLACEMENT_3D ( 'NONE', #6498, #6856, #14948 ) ;
#1833=EDGE_CURVE ( 'NONE', #209, #6280, #4137, .T. ) ;
#1865=CARTESIAN_POINT ( 'NONE',  ( 4.121423858225409909, -12.61643262889541894, 0.000000000000000000 ) ) ;
#1922=CARTESIAN_POINT ( 'NONE',  ( -6.938893903907228378E-15, 0.7408941433508786645, -1.200000000000006617 ) ) ;
#1929=FACE_OUTER_BOUND ( 'NONE', #31203, .T. ) ;
#1933=CARTESIAN_POINT ( 'NONE',  ( -3.983177536951265640, -13.66651769228263724, 0.000000000000000000 ) ) ;
#1936=DIRECTION ( 'NONE',  ( 1.783119874454246424E-31, 1.187911941725854497E-31, -1.000000000000000000 ) ) ;
#1967=VECTOR ( 'NONE', #12919, 1000.000000000000000 ) ;
#2003=ORIENTED_EDGE ( 'NONE', *, *, #8806, .F. ) ;
#2015=FACE_OUTER_BOUND ( 'NONE', #31439, .T. ) ;
#2026=ORIENTED_EDGE ( 'NONE', *, *, #21631, .T. ) ;
#2050=ORIENTED_EDGE ( 'NONE', *, *, #20408, .T. ) ;
#2098=DIRECTION ( 'NONE',  ( -1.783119874454246424E-31, -1.187911941725854497E-31, 1.000000000000000000 ) ) ;
#2131=STYLED_ITEM ( 'NONE', ( #16410 ), #34958 ) ;
#2133=DIRECTION ( 'NONE',  ( 1.000000000000000000, 0.000000000000000000, 0.000000000000000000 ) ) ;
#2138=DIRECTION ( 'NONE',  ( -1.783119874454246424E-31, -1.187911941725854497E-31, 1.000000000000000000 ) ) ;
#2200=ORIENTED_EDGE ( 'NONE', *, *, #30624, .T. ) ;
#2206=AXIS2_PLACEMENT_3D ( 'NONE', #1609, #34195, #28792 ) ;
#2291=ADVANCED_FACE ( 'NONE', ( #17924 ), #9471, .F. ) ;
#2306=CARTESIAN_POINT ( 'NONE',  ( -4.121423858225413461, -12.61643262889540473, 0.000000000000000000 ) ) ;
#2368=ORIENTED_EDGE ( 'NONE', *, *, #29562, .F. ) ;
#2473=AXIS2_PLACEMENT_3D ( 'NONE', #11702, #11181, #32975 ) ;
#2486=CIRCLE ( 'NONE', #34683, 0.7500000000000006661 ) ;
#2495=DIRECTION ( 'NONE',  ( -1.783119874454246424E-31, -1.187911941725854497E-31, 1.000000000000000000 ) ) ;
#2519=CARTESIAN_POINT ( 'NONE',  ( -2.600000000000004530, -12.74999999999999822, -1.200000000000006617 ) ) ;
#2729=VERTEX_POINT ( 'NONE', #265 ) ;
#2732=VECTOR ( 'NONE', #6441, 1000.000000000000000 ) ;
#2780=( NAMED_UNIT ( * ) PLANE_ANGLE_UNIT ( ) SI_UNIT ( $, .RADIAN. ) );
#2798=DIRECTION ( 'NONE',  ( -1.783119874454246424E-31, -1.187911941725854497E-31, 1.000000000000000000 ) ) ;
#2943=ADVANCED_FACE ( 'NONE', ( #26546 ), #12681, .T. ) ;
#3016=CYLINDRICAL_SURFACE ( 'NONE', #35475, 12.55910585664918422 ) ;
#3059=ORIENTED_EDGE ( 'NONE', *, *, #17897, .F. ) ;
#3156=AXIS2_PLACEMENT_3D ( 'NONE', #20079, #22969, #1029 ) ;
#3163=ORIENTED_EDGE ( 'NONE', *, *, #21065, .T. ) ;
#3189=CARTESIAN_POINT ( 'NONE',  ( 5.639656061357297467, -10.48075544252193048, -1.200000000000006617 ) ) ;
#3272=( GEOMETRIC_REPRESENTATION_CONTEXT ( 3 ) GLOBAL_UNCERTAINTY_ASSIGNED_CONTEXT ( ( #25453 ) ) GLOBAL_UNIT_ASSIGNED_CONTEXT ( ( #11202, #2780, #8505 ) ) REPRESENTATION_CONTEXT ( 'NONE', 'WORKASPACE' ) );
#3298=EDGE_CURVE ( 'NONE', #33119, #14640, #18746, .T. ) ;
#3369=ADVANCED_FACE ( 'NONE', ( #3622 ), #27753, .F. ) ;
#3371=CIRCLE ( 'NONE', #5680, 2.799122904894268071 ) ;
#3408=FACE_BOUND ( 'NONE', #9795, .T. ) ;
#3590=DIRECTION ( 'NONE',  ( 1.000000000000000000, 0.000000000000000000, 0.000000000000000000 ) ) ;
#3622=FACE_OUTER_BOUND ( 'NONE', #27621, .T. ) ;
#3625=CYLINDRICAL_SURFACE ( 'NONE', #30922, 10.50000000000000178 ) ;
#3650=ORIENTED_EDGE ( 'NONE', *, *, #29562, .T. ) ;
#3722=CARTESIAN_POINT ( 'NONE',  ( 4.121423858225409909, -12.61643262889541894, -1.200000000000006617 ) ) ;
#3806=CARTESIAN_POINT ( 'NONE',  ( -3.983177536951265640, -13.66651769228263724, -1.200000000000006617 ) ) ;
#3882=AXIS2_PLACEMENT_3D ( 'NONE', #29379, #16190, #26505 ) ;
#3904=AXIS2_PLACEMENT_3D ( 'NONE', #29304, #23350, #2133 ) ;
#3923=CIRCLE ( 'NONE', #21170, 1.000000000000000444 ) ;
#3931=ORIENTED_EDGE ( 'NONE', *, *, #8792, .F. ) ;
#3936=DIRECTION ( 'NONE',  ( 1.783119874454246424E-31, 1.187911941725854497E-31, -1.000000000000000000 ) ) ;
#4040=VERTEX_POINT ( 'NONE', #11491 ) ;
#4115=DIRECTION ( 'NONE',  ( 1.000000000000000000, 0.000000000000000000, 0.000000000000000000 ) ) ;
#4137=LINE ( 'NONE', #6988, #4291 ) ;
#4285=CARTESIAN_POINT ( 'NONE',  ( 12.55910585664917711, 0.7408941433508786645, -1.155557966632341512E-29 ) ) ;
#4291=VECTOR ( 'NONE', #23376, 1000.000000000000000 ) ;
#4315=VERTEX_POINT ( 'NONE', #113 ) ;
#4386=DIRECTION ( 'NONE',  ( 0.1305261922200496583, 0.9914448613738107152, -1.707538432754661574E-31 ) ) ;
#4467=ORIENTED_EDGE ( 'NONE', *, *, #14824, .F. ) ;
#4544=ORIENTED_EDGE ( 'NONE', *, *, #13246, .F. ) ;
#4549=DIRECTION ( 'NONE',  ( -1.783119874454246424E-31, -1.187911941725854497E-31, 1.000000000000000000 ) ) ;
#4550=CARTESIAN_POINT ( 'NONE',  ( 0.2142857142857085284, -10.49781318335649161, -1.200000000000006617 ) ) ;
#4636=DIRECTION ( 'NONE',  ( 1.000000000000000000, 0.000000000000000000, -1.691777834109591064E-31 ) ) ;
#4690=DIRECTION ( 'NONE',  ( -1.783119874454246424E-31, -1.187911941725854497E-31, 1.000000000000000000 ) ) ;
#4694=VECTOR ( 'NONE', #4549, 1000.000000000000000 ) ;
#4748=LINE ( 'NONE', #12835, #30758 ) ;
#4794=CYLINDRICAL_SURFACE ( 'NONE', #22795, 2.799122904894268071 ) ;
#4799=EDGE_LOOP ( 'NONE', ( #26119, #27654, #34244, #26720 ) ) ;
#4821=DIRECTION ( 'NONE',  ( -1.783119874454246424E-31, -1.187911941725854497E-31, 1.000000000000000000 ) ) ;
#4822=AXIS2_PLACEMENT_3D ( 'NONE', #11490, #25363, #14889 ) ;
#4841=EDGE_CURVE ( 'NONE', #29049, #18180, #7708, .T. ) ;
#4873=VERTEX_POINT ( 'NONE', #3806 ) ;
#4915=AXIS2_PLACEMENT_3D ( 'NONE', #33256, #2495, #19544 ) ;
#4929=FACE_OUTER_BOUND ( 'NONE', #25889, .T. ) ;
#4942=CARTESIAN_POINT ( 'NONE',  ( -0.6000000000000037526, -12.74999999999999822, -1.200000000000006617 ) ) ;
#4950=LINE ( 'NONE', #7806, #33755 ) ;
#5066=ORIENTED_EDGE ( 'NONE', *, *, #8119, .T. ) ;
#5087=DIRECTION ( 'NONE',  ( -1.783119874454246424E-31, -1.187911941725854497E-31, 1.000000000000000000 ) ) ;
#5213=DIRECTION ( 'NONE',  ( 1.000000000000000000, 0.000000000000000000, 0.000000000000000000 ) ) ;
#5385=DIRECTION ( 'NONE',  ( -1.783119874454246424E-31, -1.187911941725854497E-31, 1.000000000000000000 ) ) ;
#5471=DIRECTION ( 'NONE',  ( 1.691777834109591064E-31, -1.187911941725854715E-31, 1.000000000000000000 ) ) ;
#5483=DIRECTION ( 'NONE',  ( 1.783119874454246424E-31, 1.187911941725854497E-31, -1.000000000000000000 ) ) ;
#5680=AXIS2_PLACEMENT_3D ( 'NONE', #11738, #16948, #24905 ) ;
#5698=CARTESIAN_POINT ( 'NONE',  ( -5.639656061357301020, -10.48075544252181857, -1.200000000000006617 ) ) ;
#5730=CARTESIAN_POINT ( 'NONE',  ( -0.2142857142857362840, -10.49781318335649161, -1.200000000000006617 ) ) ;
#5757=DIRECTION ( 'NONE',  ( -1.783119874454246424E-31, -1.187911941725854497E-31, 1.000000000000000000 ) ) ;
#5782=VERTEX_POINT ( 'NONE', #3189 ) ;
#5800=ORIENTED_EDGE ( 'NONE', *, *, #16313, .T. ) ;
#5897=SHAPE_DEFINITION_REPRESENTATION ( #15253, #30285 ) ;
#5907=UNCERTAINTY_MEASURE_WITH_UNIT (LENGTH_MEASURE( 1.000000000000000082E-05 ), #19257, 'distance_accuracy_value', 'NONE');
#5914=DIRECTION ( 'NONE',  ( -1.783119874454246424E-31, -1.187911941725854497E-31, 1.000000000000000000 ) ) ;
#5949=AXIS2_PLACEMENT_3D ( 'NONE', #31749, #15706, #20751 ) ;
#6071=CARTESIAN_POINT ( 'NONE',  ( 0.000000000000000000, 0.000000000000000000, -1.200000000000006617 ) ) ;
#6088=DIRECTION ( 'NONE',  ( 0.9997917317482359900, -0.02040816326530624225, -1.905159032394999552E-31 ) ) ;
#6170=EDGE_CURVE ( 'NONE', #6280, #10552, #29448, .T. ) ;
#6250=DIRECTION ( 'NONE',  ( 1.000000000000000000, 0.000000000000000000, 0.000000000000000000 ) ) ;
#6280=VERTEX_POINT ( 'NONE', #24931 ) ;
#6352=CARTESIAN_POINT ( 'NONE',  ( 0.000000000000000000, 0.000000000000000000, -1.200000000000006617 ) ) ;
#6379=ORIENTED_EDGE ( 'NONE', *, *, #34167, .T. ) ;
#6441=DIRECTION ( 'NONE',  ( -1.783119874454246424E-31, -1.187911941725854497E-31, 1.000000000000000000 ) ) ;
#6467=FILL_AREA_STYLE_COLOUR ( '', #550 ) ;
#6474=DIRECTION ( 'NONE',  ( 1.000000000000000000, 0.000000000000000000, -1.691777834109591502E-31 ) ) ;
#6498=CARTESIAN_POINT ( 'NONE',  ( 1.600000000000004086, -12.74999999999999822, -1.200000000000006617 ) ) ;
#6584=DIRECTION ( 'NONE',  ( 1.000000000000000000, 0.000000000000000000, 0.000000000000000000 ) ) ;
#6676=DIRECTION ( 'NONE',  ( -0.9997917317482359900, -0.02040816326530611735, 3.453951567998058470E-31 ) ) ;
#6681=CARTESIAN_POINT ( 'NONE',  ( 3.239593890920905217, -13.56862304811760822, -1.200000000000006617 ) ) ;
#6759=CIRCLE ( 'NONE', #21692, 0.7500000000000006661 ) ;
#6856=DIRECTION ( 'NONE',  ( -1.783119874454246424E-31, -1.187911941725854497E-31, 1.000000000000000000 ) ) ;
#6937=CARTESIAN_POINT ( 'NONE',  ( -6.938893903907228378E-15, 0.7408941433508786645, -1.200000000000006617 ) ) ;
#6988=CARTESIAN_POINT ( 'NONE',  ( 0.2142857142857085284, -10.49781318335649161, -1.200000000000006617 ) ) ;
#6991=ORIENTED_EDGE ( 'NONE', *, *, #12379, .T. ) ;
#6997=( LENGTH_UNIT ( ) NAMED_UNIT ( * ) SI_UNIT ( .MILLI., .METRE. ) );
#7002=CARTESIAN_POINT ( 'NONE',  ( 3.239593890920905217, -13.56862304811760822, 0.000000000000000000 ) ) ;
#7116=CARTESIAN_POINT ( 'NONE',  ( 2.600000000000004974, -12.74999999999999822, -1.200000000000006617 ) ) ;
#7153=CARTESIAN_POINT ( 'NONE',  ( 0.000000000000000000, 0.000000000000000000, -1.200000000000006617 ) ) ;
#7240=DIRECTION ( 'NONE',  ( -1.783119874454246424E-31, -1.187911941725854497E-31, 1.000000000000000000 ) ) ;
#7303=ORIENTED_EDGE ( 'NONE', *, *, #35204, .T. ) ;
#7332=CARTESIAN_POINT ( 'NONE',  ( 2.600000000000004974, -12.74999999999999822, -1.691777834109592378E-31 ) ) ;
#7409=LINE ( 'NONE', #13, #10973 ) ;
#7490=AXIS2_PLACEMENT_3D ( 'NONE', #28335, #25642, #17155 ) ;
#7503=EDGE_CURVE ( 'NONE', #4040, #23706, #4950, .T. ) ;
#7544=CIRCLE ( 'NONE', #23059, 12.55910585664918422 ) ;
#7708=CIRCLE ( 'NONE', #27847, 10.50000000000000178 ) ;
#7778=ADVANCED_FACE ( 'NONE', ( #26605 ), #12914, .F. ) ;
#7806=CARTESIAN_POINT ( 'NONE',  ( 0.6000000000000035305, -12.74999999999999822, -1.200000000000006617 ) ) ;
#7811=VERTEX_POINT ( 'NONE', #7332 ) ;
#7894=VECTOR ( 'NONE', #4821, 1000.000000000000000 ) ;
#7946=AXIS2_PLACEMENT_3D ( 'NONE', #23889, #10204, #21173 ) ;
#7964=LINE ( 'NONE', #27067, #27663 ) ;
#7977=DIRECTION ( 'NONE',  ( -1.783119874454246424E-31, -1.187911941725854497E-31, 1.000000000000000000 ) ) ;
#8058=CIRCLE ( 'NONE', #7490, 10.50000000000000178 ) ;
#8103=AXIS2_PLACEMENT_3D ( 'NONE', #11198, #22170, #15875 ) ;
#8119=EDGE_CURVE ( 'NONE', #4873, #33119, #6759, .T. ) ;
#8136=DIRECTION ( 'NONE',  ( 0.1305261922200512403, -0.9914448613738104932, 6.326001338775677127E-32 ) ) ;
#8141=VERTEX_POINT ( 'NONE', #8651 ) ;
#8201=ADVANCED_FACE ( 'NONE', ( #28106 ), #3625, .F. ) ;
#8216=CIRCLE ( 'NONE', #21990, 14.70000000000000107 ) ;
#8246=ORIENTED_EDGE ( 'NONE', *, *, #33739, .F. ) ;
#8256=LINE ( 'NONE', #9452, #23092 ) ;
#8307=PLANE ( 'NONE',  #8103 ) ;
#8354=CARTESIAN_POINT ( 'NONE',  ( -3.413765605486555721, -14.29811891091961584, 0.000000000000000000 ) ) ;
#8451=CIRCLE ( 'NONE', #19360, 12.55910585664918422 ) ;
#8504=ORIENTED_EDGE ( 'NONE', *, *, #24020, .F. ) ;
#8505=( NAMED_UNIT ( * ) SI_UNIT ( $, .STERADIAN. ) SOLID_ANGLE_UNIT ( ) );
#8638=CIRCLE ( 'NONE', #28184, 10.50000000000000178 ) ;
#8651=CARTESIAN_POINT ( 'NONE',  ( 2.600000000000004974, -12.74999999999999822, -1.200000000000006617 ) ) ;
#8695=APPLICATION_CONTEXT ( 'automotive_design' ) ;
#8720=CARTESIAN_POINT ( 'NONE',  ( -4.121423858225413461, -12.61643262889540473, -1.200000000000006617 ) ) ;
#8753=EDGE_LOOP ( 'NONE', ( #23857, #22410, #26439, #21904 ) ) ;
#8770=DIRECTION ( 'NONE',  ( 0.02040816326530617286, -0.9997917317482359900, 9.329158281316450075E-32 ) ) ;
#8771=UNCERTAINTY_MEASURE_WITH_UNIT (LENGTH_MEASURE( 1.000000000000000082E-05 ), #6997, 'distance_accuracy_value', 'NONE');
#8792=EDGE_CURVE ( 'NONE', #4315, #28212, #9325, .T. ) ;
#8806=EDGE_CURVE ( 'NONE', #18916, #11231, #1404, .T. ) ;
#8872=DIRECTION ( 'NONE',  ( -1.783119874454246424E-31, -1.187911941725854497E-31, 1.000000000000000000 ) ) ;
#8884=ADVANCED_FACE ( 'NONE', ( #23720 ), #10036, .T. ) ;
#8887=ORIENTED_EDGE ( 'NONE', *, *, #26894, .F. ) ;
#8933=EDGE_LOOP ( 'NONE', ( #15478, #4467, #5066, #10130 ) ) ;
#9019=EDGE_LOOP ( 'NONE', ( #34553, #11709, #7303, #17284 ) ) ;
#9077=ORIENTED_EDGE ( 'NONE', *, *, #23320, .T. ) ;
#9120=ORIENTED_EDGE ( 'NONE', *, *, #22524, .T. ) ;
#9132=CARTESIAN_POINT ( 'NONE',  ( -1.600000000000004086, -12.74999999999999822, 0.000000000000000000 ) ) ;
#9152=CARTESIAN_POINT ( 'NONE',  ( 10.50000000000000178, -7.127471650355116251E-32, -1.200000000000006617 ) ) ;
#9198=EDGE_LOOP ( 'NONE', ( #17887, #18571, #32648, #1417, #9077, #32506, #25376, #24844, #35228, #32942, #27728, #33471, #6991, #31836, #3650, #13911 ) ) ;
#9203=VERTEX_POINT ( 'NONE', #24965 ) ;
#9214=VECTOR ( 'NONE', #17484, 1000.000000000000000 ) ;
#9275=DIRECTION ( 'NONE',  ( -1.783119874454246424E-31, -1.187911941725854497E-31, 1.000000000000000000 ) ) ;
#9296=VERTEX_POINT ( 'NONE', #21141 ) ;
#9325=LINE ( 'NONE', #28241, #2732 ) ;
#9349=SHAPE_REPRESENTATION_RELATIONSHIP ( 'NONE' , 'NONE' ,  #30285, #487 ) ;
#9452=CARTESIAN_POINT ( 'NONE',  ( 4.121423858225409909, -12.61643262889541894, -1.200000000000006617 ) ) ;
#9471=CYLINDRICAL_SURFACE ( 'NONE', #3156, 10.50000000000000178 ) ;
#9486=DIRECTION ( 'NONE',  ( -1.783119874454246424E-31, -1.187911941725854497E-31, 1.000000000000000000 ) ) ;
#9490=CARTESIAN_POINT ( 'NONE',  ( 0.000000000000000000, 0.000000000000000000, -1.200000000000006617 ) ) ;
#9566=DIRECTION ( 'NONE',  ( -1.000000000000000000, 0.000000000000000000, 0.000000000000000000 ) ) ;
#9597=CYLINDRICAL_SURFACE ( 'NONE', #30079, 1.000000000000000444 ) ;
#9684=CIRCLE ( 'NONE', #29828, 12.55910585664918422 ) ;
#9738=LINE ( 'NONE', #17654, #4694 ) ;
#9785=ORIENTED_EDGE ( 'NONE', *, *, #12379, .F. ) ;
#9795=EDGE_LOOP ( 'NONE', ( #16396, #26048 ) ) ;
#10026=ORIENTED_EDGE ( 'NONE', *, *, #14824, .T. ) ;
#10036=CYLINDRICAL_SURFACE ( 'NONE', #32595, 14.70000000000000107 ) ;
#10081=CLOSED_SHELL ( 'NONE', ( #14335, #3369, #29311, #15692, #8201, #16052, #2291, #23787, #19167, #25612, #11330, #28969, #13259, #7778, #14679, #2943, #8884, #1335, #23807, #16766, #30406, #23101 ) ) ;
#10130=ORIENTED_EDGE ( 'NONE', *, *, #3298, .T. ) ;
#10196=ORIENTED_EDGE ( 'NONE', *, *, #10564, .T. ) ;
#10204=DIRECTION ( 'NONE',  ( -1.783119874454246424E-31, -1.187911941725854497E-31, 1.000000000000000000 ) ) ;
#10497=CARTESIAN_POINT ( 'NONE',  ( -3.983177536951265640, -13.66651769228263724, -1.200000000000006617 ) ) ;
#10533=DIRECTION ( 'NONE',  ( 0.02040816326530624572, 0.9997917317482359900, -1.513872302914096262E-31 ) ) ;
#10552=VERTEX_POINT ( 'NONE', #12528 ) ;
#10564=EDGE_CURVE ( 'NONE', #8141, #7811, #34677, .T. ) ;
#10565=LINE ( 'NONE', #34890, #7894 ) ;
#10574=FACE_OUTER_BOUND ( 'NONE', #23047, .T. ) ;
#10652=ORIENTED_EDGE ( 'NONE', *, *, #24181, .T. ) ;
#10714=DIRECTION ( 'NONE',  ( 0.02040816326530617286, -0.9997917317482359900, 9.329158281316450075E-32 ) ) ;
#10966=EDGE_CURVE ( 'NONE', #31461, #19641, #8058, .T. ) ;
#10973=VECTOR ( 'NONE', #26689, 1000.000000000000000 ) ;
#11104=LINE ( 'NONE', #5698, #32959 ) ;
#11134=AXIS2_PLACEMENT_3D ( 'NONE', #1226, #6088, #28592 ) ;
#11181=DIRECTION ( 'NONE',  ( -1.783119874454246424E-31, -1.187911941725854497E-31, 1.000000000000000000 ) ) ;
#11193=AXIS2_PLACEMENT_3D ( 'NONE', #13686, #5757, #21948 ) ;
#11198=CARTESIAN_POINT ( 'NONE',  ( -4.121423858225413461, -12.61643262889540473, -1.200000000000006617 ) ) ;
#11202=( LENGTH_UNIT ( ) NAMED_UNIT ( * ) SI_UNIT ( .MILLI., .METRE. ) );
#11231=VERTEX_POINT ( 'NONE', #19475 ) ;
#11259=EDGE_CURVE ( 'NONE', #29210, #18916, #27605, .T. ) ;
#11261=EDGE_CURVE ( 'NONE', #33467, #4873, #7964, .T. ) ;
#11296=ORIENTED_EDGE ( 'NONE', *, *, #17360, .F. ) ;
#11302=AXIS2_PLACEMENT_3D ( 'NONE', #31037, #28513, #34099 ) ;
#11306=PRODUCT_CONTEXT ( 'NONE', #8695, 'mechanical' ) ;
#11330=ADVANCED_FACE ( 'NONE', ( #4929 ), #8307, .T. ) ;
#11410=DIRECTION ( 'NONE',  ( 1.000000000000000000, 0.000000000000000000, -1.691777834109590845E-31 ) ) ;
#11435=ORIENTED_EDGE ( 'NONE', *, *, #33739, .T. ) ;
#11471=AXIS2_PLACEMENT_3D ( 'NONE', #9490, #3936, #31279 ) ;
#11490=CARTESIAN_POINT ( 'NONE',  ( 0.000000000000000000, 0.000000000000000000, -1.200000000000006617 ) ) ;
#11491=CARTESIAN_POINT ( 'NONE',  ( 0.6000000000000035305, -12.74999999999999822, -1.200000000000006617 ) ) ;
#11507=EDGE_CURVE ( 'NONE', #4040, #8141, #29405, .T. ) ;
#11544=EDGE_LOOP ( 'NONE', ( #14240, #34521, #5800, #980 ) ) ;
#11570=EDGE_CURVE ( 'NONE', #19641, #29049, #9738, .T. ) ;
#11587=LINE ( 'NONE', #780, #19140 ) ;
#11632=DIRECTION ( 'NONE',  ( -1.783119874454246424E-31, -1.187911941725854497E-31, 1.000000000000000000 ) ) ;
#11702=CARTESIAN_POINT ( 'NONE',  ( 1.600000000000004086, -12.74999999999999822, -1.200000000000006617 ) ) ;
#11709=ORIENTED_EDGE ( 'NONE', *, *, #26305, .F. ) ;
#11738=CARTESIAN_POINT ( 'NONE',  ( -6.896599878636569869, -12.98179148322720167, -1.200000000000006617 ) ) ;
#11878=VECTOR ( 'NONE', #21107, 1000.000000000000000 ) ;
#11890=EDGE_CURVE ( 'NONE', #580, #35153, #30570, .T. ) ;
#12027=CARTESIAN_POINT ( 'NONE',  ( -0.2142857142857362840, -10.49781318335649161, 0.000000000000000000 ) ) ;
#12053=EDGE_CURVE ( 'NONE', #2729, #15714, #25980, .T. ) ;
#12179=EDGE_CURVE ( 'NONE', #9296, #17469, #24287, .T. ) ;
#12235=VERTEX_POINT ( 'NONE', #4285 ) ;
#12379=EDGE_CURVE ( 'NONE', #35153, #31912, #26964, .T. ) ;
#12527=CARTESIAN_POINT ( 'NONE',  ( -6.896599878636569869, -12.98179148322720167, -1.200000000000006617 ) ) ;
#12528=CARTESIAN_POINT ( 'NONE',  ( 0.3000000000000016542, -14.69693845669907439, 0.000000000000000000 ) ) ;
#12544=EDGE_CURVE ( 'NONE', #18180, #6280, #8638, .T. ) ;
#12545=CARTESIAN_POINT ( 'NONE',  ( 0.000000000000000000, 0.000000000000000000, 0.000000000000000000 ) ) ;
#12677=ORIENTED_EDGE ( 'NONE', *, *, #19432, .F. ) ;
#12681=CYLINDRICAL_SURFACE ( 'NONE', #5949, 0.7500000000000006661 ) ;
#12725=DIRECTION ( 'NONE',  ( 0.000000000000000000, 0.000000000000000000, 1.000000000000000000 ) ) ;
#12741=CARTESIAN_POINT ( 'NONE',  ( 12.55910585664917711, 0.7408941433508786645, -1.200000000000006617 ) ) ;
#12778=CARTESIAN_POINT ( 'NONE',  ( 6.896599878636562764, -12.98179148322720167, 0.000000000000000000 ) ) ;
#12796=ORIENTED_EDGE ( 'NONE', *, *, #12809, .T. ) ;
#12809=EDGE_CURVE ( 'NONE', #5782, #31873, #30582, .T. ) ;
#12835=CARTESIAN_POINT ( 'NONE',  ( 10.50000000000000178, 0.000000000000000000, -1.200000000000006617 ) ) ;
#12848=EDGE_CURVE ( 'NONE', #5782, #14643, #32218, .T. ) ;
#12914=CYLINDRICAL_SURFACE ( 'NONE', #3904, 2.799122904894268071 ) ;
#12919=DIRECTION ( 'NONE',  ( -1.783119874454246424E-31, -1.187911941725854497E-31, 1.000000000000000000 ) ) ;
#13023=ORIENTED_EDGE ( 'NONE', *, *, #12053, .F. ) ;
#13048=CARTESIAN_POINT ( 'NONE',  ( 0.000000000000000000, 0.000000000000000000, 0.000000000000000000 ) ) ;
#13075=DIRECTION ( 'NONE',  ( 1.000000000000000000, 0.000000000000000000, 0.000000000000000000 ) ) ;
#13102=VERTEX_POINT ( 'NONE', #31818 ) ;
#13246=EDGE_CURVE ( 'NONE', #31873, #12235, #34536, .T. ) ;
#13259=ADVANCED_FACE ( 'NONE', ( #10574 ), #3016, .T. ) ;
#13277=DIRECTION ( 'NONE',  ( 0.1305261922200512403, -0.9914448613738104932, 6.326001338775677127E-32 ) ) ;
#13499=CARTESIAN_POINT ( 'NONE',  ( 5.639656061357297467, -10.48075544252193048, -1.200000000000006617 ) ) ;
#13561=AXIS2_PLACEMENT_3D ( 'NONE', #6352, #19659, #30672 ) ;
#13651=CIRCLE ( 'NONE', #19359, 0.7500000000000006661 ) ;
#13686=CARTESIAN_POINT ( 'NONE',  ( -3.239593890920919428, -13.56862304811759579, 0.000000000000000000 ) ) ;
#13741=SURFACE_SIDE_STYLE ('',( #27431 ) ) ;
#13763=DIRECTION ( 'NONE',  ( 1.000000000000000000, 0.000000000000000000, -1.691777834109591064E-31 ) ) ;
#13833=CIRCLE ( 'NONE', #15536, 2.799122904894268071 ) ;
#13873=ORIENTED_EDGE ( 'NONE', *, *, #20534, .T. ) ;
#13897=EDGE_LOOP ( 'NONE', ( #3059, #19067, #26691, #11435 ) ) ;
#13911=ORIENTED_EDGE ( 'NONE', *, *, #8806, .T. ) ;
#13915=ORIENTED_EDGE ( 'NONE', *, *, #11570, .T. ) ;
#13975=DIRECTION ( 'NONE',  ( 1.000000000000000000, 0.000000000000000000, 0.000000000000000000 ) ) ;
#14006=AXIS2_PLACEMENT_3D ( 'NONE', #4550, #6676, #15481 ) ;
#14240=ORIENTED_EDGE ( 'NONE', *, *, #11890, .F. ) ;
#14254=ORIENTED_EDGE ( 'NONE', *, *, #26180, .T. ) ;
#14281=EDGE_CURVE ( 'NONE', #9203, #25659, #28915, .T. ) ;
#14335=ADVANCED_FACE ( 'NONE', ( #32862 ), #18457, .F. ) ;
#14356=FACE_BOUND ( 'NONE', #14699, .T. ) ;
#14386=EDGE_LOOP ( 'NONE', ( #20519, #21427, #19803, #34472 ) ) ;
#14408=VECTOR ( 'NONE', #8770, 1000.000000000000114 ) ;
#14574=CIRCLE ( 'NONE', #19730, 1.000000000000000888 ) ;
#14640=VERTEX_POINT ( 'NONE', #8354 ) ;
#14643=VERTEX_POINT ( 'NONE', #30346 ) ;
#14676=ORIENTED_EDGE ( 'NONE', *, *, #26180, .F. ) ;
#14679=ADVANCED_FACE ( 'NONE', ( #14994 ), #23098, .T. ) ;
#14699=EDGE_LOOP ( 'NONE', ( #6379, #23245 ) ) ;
#14739=( NAMED_UNIT ( * ) SI_UNIT ( $, .STERADIAN. ) SOLID_ANGLE_UNIT ( ) );
#14824=EDGE_CURVE ( 'NONE', #4873, #31912, #16051, .T. ) ;
#14861=EDGE_LOOP ( 'NONE', ( #2003, #33729, #14254, #2200 ) ) ;
#14889=DIRECTION ( 'NONE',  ( 1.000000000000000000, 0.000000000000000000, -1.691777834109591064E-31 ) ) ;
#14892=CARTESIAN_POINT ( 'NONE',  ( -6.938893903907228378E-15, 0.7408941433508786645, -1.200000000000006617 ) ) ;
#14916=ORIENTED_EDGE ( 'NONE', *, *, #29991, .T. ) ;
#14931=CARTESIAN_POINT ( 'NONE',  ( 0.000000000000000000, 0.000000000000000000, -1.200000000000006617 ) ) ;
#14945=ORIENTED_EDGE ( 'NONE', *, *, #21631, .F. ) ;
#14948=DIRECTION ( 'NONE',  ( 1.000000000000000000, 0.000000000000000000, 0.000000000000000000 ) ) ;
#14994=FACE_OUTER_BOUND ( 'NONE', #787, .T. ) ;
#14996=DIRECTION ( 'NONE',  ( -1.783119874454246424E-31, -1.187911941725854497E-31, 1.000000000000000000 ) ) ;
#15074=VERTEX_POINT ( 'NONE', #33514 ) ;
#15122=CARTESIAN_POINT ( 'NONE',  ( -4.121423858225413461, -12.61643262889540473, 0.000000000000000000 ) ) ;
#15133=LINE ( 'NONE', #25966, #9214 ) ;
#15234=LINE ( 'NONE', #12741, #1967 ) ;
#15251=ORIENTED_EDGE ( 'NONE', *, *, #27246, .T. ) ;
#15253=PRODUCT_DEFINITION_SHAPE ( 'NONE', 'NONE',  #27561 ) ;
#15321=MECHANICAL_DESIGN_GEOMETRIC_PRESENTATION_REPRESENTATION('',(#2131),#3272);
#15392=DIRECTION ( 'NONE',  ( -1.783119874454246424E-31, -1.187911941725854497E-31, 1.000000000000000000 ) ) ;
#15478=ORIENTED_EDGE ( 'NONE', *, *, #26638, .F. ) ;
#15481=DIRECTION ( 'NONE',  ( 0.02040816326530611735, -0.9997917317482359900, 1.302694377452200301E-31 ) ) ;
#15536=AXIS2_PLACEMENT_3D ( 'NONE', #30667, #25085, #413 ) ;
#15573=CYLINDRICAL_SURFACE ( 'NONE', #7946, 14.70000000000000107 ) ;
#15580=CARTESIAN_POINT ( 'NONE',  ( -12.55910585664919132, 0.7408941433508802188, -1.200000000000006617 ) ) ;
#15613=CARTESIAN_POINT ( 'NONE',  ( -0.6000000000000037526, -12.74999999999999822, -1.691777834109591940E-31 ) ) ;
#15692=ADVANCED_FACE ( 'NONE', ( #29867 ), #1610, .T. ) ;
#15706=DIRECTION ( 'NONE',  ( -1.783119874454246424E-31, -1.187911941725854497E-31, 1.000000000000000000 ) ) ;
#15714=VERTEX_POINT ( 'NONE', #15613 ) ;
#15794=CIRCLE ( 'NONE', #4915, 1.000000000000000888 ) ;
#15875=DIRECTION ( 'NONE',  ( 0.1305261922200510738, -0.9914448613738104932, 1.248897716083276957E-31 ) ) ;
#16051=LINE ( 'NONE', #10497, #11878 ) ;
#16052=ADVANCED_FACE ( 'NONE', ( #31452 ), #33981, .F. ) ;
#16054=CIRCLE ( 'NONE', #11471, 10.50000000000000178 ) ;
#16190=DIRECTION ( 'NONE',  ( -1.783119874454246424E-31, -1.187911941725854497E-31, 1.000000000000000000 ) ) ;
#16304=CARTESIAN_POINT ( 'NONE',  ( -3.239593890920919428, -13.56862304811759579, -1.200000000000006617 ) ) ;
#16313=EDGE_CURVE ( 'NONE', #13102, #33467, #3371, .T. ) ;
#16330=ORIENTED_EDGE ( 'NONE', *, *, #34208, .F. ) ;
#16396=ORIENTED_EDGE ( 'NONE', *, *, #12179, .T. ) ;
#16410=PRESENTATION_STYLE_ASSIGNMENT (( #25249 ) ) ;
#16418=DIRECTION ( 'NONE',  ( -1.783119874454246424E-31, -1.187911941725854497E-31, 1.000000000000000000 ) ) ;
#16761=EDGE_LOOP ( 'NONE', ( #20864, #27345, #4544, #307 ) ) ;
#16766=ADVANCED_FACE ( 'NONE', ( #29963, #24377, #27261 ), #32660, .T. ) ;
#16817=ORIENTED_EDGE ( 'NONE', *, *, #14281, .T. ) ;
#16916=CARTESIAN_POINT ( 'NONE',  ( -3.239593890920919428, -13.56862304811759579, -1.200000000000006617 ) ) ;
#16948=DIRECTION ( 'NONE',  ( 1.783119874454246424E-31, 1.187911941725854497E-31, -1.000000000000000000 ) ) ;
#17012=AXIS2_PLACEMENT_3D ( 'NONE', #33923, #14996, #20380 ) ;
#17060=DIRECTION ( 'NONE',  ( -1.783119874454246424E-31, -1.187911941725854497E-31, 1.000000000000000000 ) ) ;
#17155=DIRECTION ( 'NONE',  ( 1.000000000000000000, 0.000000000000000000, 0.000000000000000000 ) ) ;
#17173=LINE ( 'NONE', #8720, #25254 ) ;
#17281=EDGE_CURVE ( 'NONE', #19897, #15074, #22949, .T. ) ;
#17284=ORIENTED_EDGE ( 'NONE', *, *, #8792, .T. ) ;
#17299=DIRECTION ( 'NONE',  ( -1.783119874454246424E-31, -1.187911941725854497E-31, 1.000000000000000000 ) ) ;
#17360=EDGE_CURVE ( 'NONE', #25659, #31873, #1711, .T. ) ;
#17412=DIRECTION ( 'NONE',  ( 1.000000000000000000, 0.000000000000000000, 0.000000000000000000 ) ) ;
#17427=DIRECTION ( 'NONE',  ( 1.000000000000000000, 0.000000000000000000, -1.691777834109591283E-31 ) ) ;
#17469=VERTEX_POINT ( 'NONE', #2519 ) ;
#17484=DIRECTION ( 'NONE',  ( -1.783119874454246424E-31, -1.187911941725854497E-31, 1.000000000000000000 ) ) ;
#17561=ORIENTED_EDGE ( 'NONE', *, *, #20534, .F. ) ;
#17608=AXIS2_PLACEMENT_3D ( 'NONE', #16304, #21528, #119 ) ;
#17636=DIRECTION ( 'NONE',  ( 1.000000000000000000, 0.000000000000000000, 0.000000000000000000 ) ) ;
#17654=CARTESIAN_POINT ( 'NONE',  ( -10.50000000000000178, 1.285879139104719253E-15, -1.200000000000006617 ) ) ;
#17660=AXIS2_PLACEMENT_3D ( 'NONE', #25894, #23532, #4115 ) ;
#17694=EDGE_CURVE ( 'NONE', #26822, #209, #16054, .T. ) ;
#17774=EDGE_CURVE ( 'NONE', #17469, #9296, #24009, .T. ) ;
#17793=( NAMED_UNIT ( * ) SI_UNIT ( $, .STERADIAN. ) SOLID_ANGLE_UNIT ( ) );
#17837=ORIENTED_EDGE ( 'NONE', *, *, #17694, .F. ) ;
#17867=CARTESIAN_POINT ( 'NONE',  ( -1.600000000000004086, -12.74999999999999822, -1.200000000000006617 ) ) ;
#17887=ORIENTED_EDGE ( 'NONE', *, *, #35544, .T. ) ;
#17897=EDGE_CURVE ( 'NONE', #17469, #2729, #10565, .T. ) ;
#17924=FACE_OUTER_BOUND ( 'NONE', #8753, .T. ) ;
#17978=DIRECTION ( 'NONE',  ( -1.783119874454246424E-31, -1.187911941725854497E-31, 1.000000000000000000 ) ) ;
#18007=FACE_OUTER_BOUND ( 'NONE', #990, .T. ) ;
#18180=VERTEX_POINT ( 'NONE', #632 ) ;
#18209=CARTESIAN_POINT ( 'NONE',  ( -6.896599878636569869, -12.98179148322720167, 0.000000000000000000 ) ) ;
#18210=ORIENTED_EDGE ( 'NONE', *, *, #20408, .F. ) ;
#18281=ORIENTED_EDGE ( 'NONE', *, *, #35204, .F. ) ;
#18292=DIRECTION ( 'NONE',  ( 1.000000000000000000, 0.000000000000000000, 0.000000000000000000 ) ) ;
#18344=CARTESIAN_POINT ( 'NONE',  ( 0.000000000000000000, 0.000000000000000000, 0.000000000000000000 ) ) ;
#18376=APPLICATION_CONTEXT ( 'automotive_design' ) ;
#18378=CYLINDRICAL_SURFACE ( 'NONE', #3882, 12.55910585664918422 ) ;
#18416=ORIENTED_EDGE ( 'NONE', *, *, #34167, .F. ) ;
#18457=CYLINDRICAL_SURFACE ( 'NONE', #26899, 1.000000000000000444 ) ;
#18571=ORIENTED_EDGE ( 'NONE', *, *, #4841, .T. ) ;
#18633=DIRECTION ( 'NONE',  ( 1.000000000000000000, 0.000000000000000000, 0.000000000000000000 ) ) ;
#18746=LINE ( 'NONE', #26699, #21413 ) ;
#18802=CIRCLE ( 'NONE', #25135, 1.000000000000000888 ) ;
#18911=ORIENTED_EDGE ( 'NONE', *, *, #31287, .F. ) ;
#18916=VERTEX_POINT ( 'NONE', #19057 ) ;
#18919=DIRECTION ( 'NONE',  ( 1.000000000000000000, 0.000000000000000000, -1.691777834109591283E-31 ) ) ;
#18959=DIRECTION ( 'NONE',  ( 1.000000000000000000, 0.000000000000000000, 0.000000000000000000 ) ) ;
#19046=DIRECTION ( 'NONE',  ( 1.000000000000000000, 0.000000000000000000, -1.691777834109591064E-31 ) ) ;
#19057=CARTESIAN_POINT ( 'NONE',  ( -0.3000000000000016542, -14.69693845669907439, 0.000000000000000000 ) ) ;
#19067=ORIENTED_EDGE ( 'NONE', *, *, #12179, .F. ) ;
#19076=AXIS2_PLACEMENT_3D ( 'NONE', #18209, #26145, #23626 ) ;
#19140=VECTOR ( 'NONE', #30684, 1000.000000000000000 ) ;
#19167=ADVANCED_FACE ( 'NONE', ( #1929 ), #15573, .T. ) ;
#19257=( LENGTH_UNIT ( ) NAMED_UNIT ( * ) SI_UNIT ( .MILLI., .METRE. ) );
#19359=AXIS2_PLACEMENT_3D ( 'NONE', #6681, #17299, #9566 ) ;
#19360=AXIS2_PLACEMENT_3D ( 'NONE', #6937, #34674, #31428 ) ;
#19412=AXIS2_PLACEMENT_3D ( 'NONE', #31840, #26457, #5213 ) ;
#19432=EDGE_CURVE ( 'NONE', #33467, #35153, #17173, .T. ) ;
#19475=CARTESIAN_POINT ( 'NONE',  ( -0.2142857142857362840, -10.49781318335649161, 0.000000000000000000 ) ) ;
#19537=FACE_OUTER_BOUND ( 'NONE', #8933, .T. ) ;
#19544=DIRECTION ( 'NONE',  ( 1.000000000000000000, 0.000000000000000000, -1.691777834109590845E-31 ) ) ;
#19601=VERTEX_POINT ( 'NONE', #15580 ) ;
#19641=VERTEX_POINT ( 'NONE', #32882 ) ;
#19659=DIRECTION ( 'NONE',  ( 1.783119874454246424E-31, 1.187911941725854497E-31, -1.000000000000000000 ) ) ;
#19687=DIRECTION ( 'NONE',  ( -1.783119874454246424E-31, -1.187911941725854497E-31, 1.000000000000000000 ) ) ;
#19730=AXIS2_PLACEMENT_3D ( 'NONE', #29656, #8872, #11410 ) ;
#19733=ORIENTED_EDGE ( 'NONE', *, *, #8119, .F. ) ;
#19803=ORIENTED_EDGE ( 'NONE', *, *, #17281, .T. ) ;
#19897=VERTEX_POINT ( 'NONE', #22583 ) ;
#19940=CARTESIAN_POINT ( 'NONE',  ( -1.600000000000004086, -12.74999999999999822, 0.000000000000000000 ) ) ;
#20069=ORIENTED_EDGE ( 'NONE', *, *, #4841, .F. ) ;
#20079=CARTESIAN_POINT ( 'NONE',  ( 0.000000000000000000, 0.000000000000000000, -1.200000000000006617 ) ) ;
#20116=CARTESIAN_POINT ( 'NONE',  ( 0.000000000000000000, 0.000000000000000000, -1.200000000000006617 ) ) ;
#20141=DIRECTION ( 'NONE',  ( 1.783119874454246424E-31, 1.187911941725854497E-31, -1.000000000000000000 ) ) ;
#20318=VECTOR ( 'NONE', #27338, 1000.000000000000000 ) ;
#20323=DIRECTION ( 'NONE',  ( -1.783119874454246424E-31, -1.187911941725854497E-31, 1.000000000000000000 ) ) ;
#20380=DIRECTION ( 'NONE',  ( 1.000000000000000000, 0.000000000000000000, -1.691777834109591064E-31 ) ) ;
#20408=EDGE_CURVE ( 'NONE', #9203, #5782, #13833, .T. ) ;
#20431=DIRECTION ( 'NONE',  ( 1.783119874454246424E-31, 1.187911941725854497E-31, -1.000000000000000000 ) ) ;
#20460=DIRECTION ( 'NONE',  ( 0.02040816326530624572, 0.9997917317482359900, -1.513872302914096262E-31 ) ) ;
#20519=ORIENTED_EDGE ( 'NONE', *, *, #23320, .F. ) ;
#20534=EDGE_CURVE ( 'NONE', #209, #19897, #25186, .T. ) ;
#20703=ORIENTED_EDGE ( 'NONE', *, *, #30624, .F. ) ;
#20740=STYLED_ITEM ( 'NONE', ( #30960 ), #487 ) ;
#20751=DIRECTION ( 'NONE',  ( 1.000000000000000000, 0.000000000000000000, 0.000000000000000000 ) ) ;
#20864=ORIENTED_EDGE ( 'NONE', *, *, #12848, .T. ) ;
#20877=PLANE ( 'NONE',  #14006 ) ;
#20940=CIRCLE ( 'NONE', #11193, 0.7500000000000006661 ) ;
#21065=EDGE_CURVE ( 'NONE', #13102, #580, #11104, .T. ) ;
#21107=DIRECTION ( 'NONE',  ( -1.783119874454246424E-31, -1.187911941725854497E-31, 1.000000000000000000 ) ) ;
#21141=CARTESIAN_POINT ( 'NONE',  ( -0.6000000000000037526, -12.74999999999999822, -1.200000000000006617 ) ) ;
#21157=CARTESIAN_POINT ( 'NONE',  ( -1.600000000000004086, -12.74999999999999822, -1.200000000000006617 ) ) ;
#21170=AXIS2_PLACEMENT_3D ( 'NONE', #19940, #31304, #17427 ) ;
#21173=DIRECTION ( 'NONE',  ( 1.000000000000000000, 0.000000000000000000, 0.000000000000000000 ) ) ;
#21281=AXIS2_PLACEMENT_3D ( 'NONE', #14892, #17060, #17412 ) ;
#21307=AXIS2_PLACEMENT_3D ( 'NONE', #26589, #12725, #18292 ) ;
#21413=VECTOR ( 'NONE', #35335, 1000.000000000000000 ) ;
#21427=ORIENTED_EDGE ( 'NONE', *, *, #29991, .F. ) ;
#21508=ORIENTED_EDGE ( 'NONE', *, *, #7503, .F. ) ;
#21528=DIRECTION ( 'NONE',  ( -1.783119874454246424E-31, -1.187911941725854497E-31, 1.000000000000000000 ) ) ;
#21541=PRODUCT_DEFINITION_CONTEXT ( 'detailed design', #18376, 'design' ) ;
#21631=EDGE_CURVE ( 'NONE', #19641, #26822, #28514, .T. ) ;
#21692=AXIS2_PLACEMENT_3D ( 'NONE', #16916, #24700, #33153 ) ;
#21818=CARTESIAN_POINT ( 'NONE',  ( -0.3000000000000016542, -14.69693845669907439, -1.200000000000006617 ) ) ;
#21825=AXIS2_PLACEMENT_3D ( 'NONE', #12778, #20141, #6474 ) ;
#21871=ORIENTED_EDGE ( 'NONE', *, *, #10966, .F. ) ;
#21904=ORIENTED_EDGE ( 'NONE', *, *, #12544, .F. ) ;
#21918=CARTESIAN_POINT ( 'NONE',  ( 0.3000000000000016542, -14.69693845669907439, -1.200000000000006617 ) ) ;
#21948=DIRECTION ( 'NONE',  ( 1.000000000000000000, 0.000000000000000000, -1.691777834109591283E-31 ) ) ;
#21972=DIRECTION ( 'NONE',  ( 1.000000000000000000, 0.000000000000000000, 0.000000000000000000 ) ) ;
#21990=AXIS2_PLACEMENT_3D ( 'NONE', #18344, #4690, #34566 ) ;
#22135=AXIS2_PLACEMENT_3D ( 'NONE', #32653, #7977, #18959 ) ;
#22144=ORIENTED_EDGE ( 'NONE', *, *, #11261, .T. ) ;
#22170=DIRECTION ( 'NONE',  ( -0.9914448613738104932, -0.1305261922200510738, 1.844340778863525675E-31 ) ) ;
#22250=CYLINDRICAL_SURFACE ( 'NONE', #17608, 0.7500000000000006661 ) ;
#22296=CARTESIAN_POINT ( 'NONE',  ( -12.55910585664919132, 0.7408941433508802188, -8.474091755303837753E-30 ) ) ;
#22410=ORIENTED_EDGE ( 'NONE', *, *, #17694, .T. ) ;
#22468=( GEOMETRIC_REPRESENTATION_CONTEXT ( 3 ) GLOBAL_UNCERTAINTY_ASSIGNED_CONTEXT ( ( #8771 ) ) GLOBAL_UNIT_ASSIGNED_CONTEXT ( ( #6997, #28795, #14739 ) ) REPRESENTATION_CONTEXT ( 'NONE', 'WORKASPACE' ) );
#22518=ORIENTED_EDGE ( 'NONE', *, *, #11259, .T. ) ;
#22524=EDGE_CURVE ( 'NONE', #4315, #9203, #8256, .T. ) ;
#22575=ORIENTED_EDGE ( 'NONE', *, *, #22524, .F. ) ;
#22583=CARTESIAN_POINT ( 'NONE',  ( 0.3000000000000016542, -14.69693845669907439, -1.200000000000006617 ) ) ;
#22696=ORIENTED_EDGE ( 'NONE', *, *, #14281, .F. ) ;
#22795=AXIS2_PLACEMENT_3D ( 'NONE', #12527, #2098, #13075 ) ;
#22848=ORIENTED_EDGE ( 'NONE', *, *, #1833, .F. ) ;
#22870=ORIENTED_EDGE ( 'NONE', *, *, #3298, .F. ) ;
#22949=CIRCLE ( 'NONE', #27583, 14.70000000000000107 ) ;
#22969=DIRECTION ( 'NONE',  ( -1.783119874454246424E-31, -1.187911941725854497E-31, 1.000000000000000000 ) ) ;
#22975=EDGE_CURVE ( 'NONE', #28212, #25659, #29038, .T. ) ;
#22978=VECTOR ( 'NONE', #1545, 1000.000000000000000 ) ;
#23047=EDGE_LOOP ( 'NONE', ( #23517, #25530, #3163, #18911 ) ) ;
#23059=AXIS2_PLACEMENT_3D ( 'NONE', #30047, #5385, #19046 ) ;
#23092=VECTOR ( 'NONE', #23133, 1000.000000000000000 ) ;
#23098=PLANE ( 'NONE',  #11302 ) ;
#23101=ADVANCED_FACE ( 'NONE', ( #34265 ), #9597, .F. ) ;
#23133=DIRECTION ( 'NONE',  ( 0.1305261922200496583, 0.9914448613738107152, -1.707538432754661574E-31 ) ) ;
#23162=DIRECTION ( 'NONE',  ( -1.783119874454246424E-31, -1.187911941725854497E-31, 1.000000000000000000 ) ) ;
#23245=ORIENTED_EDGE ( 'NONE', *, *, #11507, .T. ) ;
#23305=EDGE_CURVE ( 'NONE', #25051, #28212, #2486, .T. ) ;
#23320=EDGE_CURVE ( 'NONE', #10552, #25051, #8216, .T. ) ;
#23323=DIRECTION ( 'NONE',  ( -1.783119874454246424E-31, -1.187911941725854497E-31, 1.000000000000000000 ) ) ;
#23350=DIRECTION ( 'NONE',  ( -1.783119874454246424E-31, -1.187911941725854497E-31, 1.000000000000000000 ) ) ;
#23376=DIRECTION ( 'NONE',  ( -1.783119874454246424E-31, -1.187911941725854497E-31, 1.000000000000000000 ) ) ;
#23504=FACE_OUTER_BOUND ( 'NONE', #11544, .T. ) ;
#23517=ORIENTED_EDGE ( 'NONE', *, *, #30915, .F. ) ;
#23532=DIRECTION ( 'NONE',  ( -1.783119874454246424E-31, -1.187911941725854497E-31, 1.000000000000000000 ) ) ;
#23626=DIRECTION ( 'NONE',  ( 1.000000000000000000, 0.000000000000000000, -1.691777834109591064E-31 ) ) ;
#23694=EDGE_LOOP ( 'NONE', ( #35052, #2026, #26043, #20069 ) ) ;
#23706=VERTEX_POINT ( 'NONE', #502 ) ;
#23708=CARTESIAN_POINT ( 'NONE',  ( -1.600000000000004086, -12.74999999999999822, -1.200000000000006617 ) ) ;
#23720=FACE_OUTER_BOUND ( 'NONE', #14386, .T. ) ;
#23787=ADVANCED_FACE ( 'NONE', ( #25189 ), #1053, .T. ) ;
#23807=ADVANCED_FACE ( 'NONE', ( #3408, #14356, #25541 ), #30577, .F. ) ;
#23857=ORIENTED_EDGE ( 'NONE', *, *, #24467, .F. ) ;
#23889=CARTESIAN_POINT ( 'NONE',  ( 0.000000000000000000, 0.000000000000000000, -1.200000000000006617 ) ) ;
#23896=DIRECTION ( 'NONE',  ( 1.000000000000000000, 0.000000000000000000, -1.691777834109591064E-31 ) ) ;
#23918=ORIENTED_EDGE ( 'NONE', *, *, #7503, .T. ) ;
#23980=ORIENTED_EDGE ( 'NONE', *, *, #17281, .F. ) ;
#24009=CIRCLE ( 'NONE', #17660, 1.000000000000000444 ) ;
#24020=EDGE_CURVE ( 'NONE', #14643, #12235, #15234, .T. ) ;
#24028=FACE_OUTER_BOUND ( 'NONE', #25164, .T. ) ;
#24181=EDGE_CURVE ( 'NONE', #7811, #23706, #14574, .T. ) ;
#24202=DIRECTION ( 'NONE',  ( 1.000000000000000000, 0.000000000000000000, -1.691777834109591064E-31 ) ) ;
#24211=( GEOMETRIC_REPRESENTATION_CONTEXT ( 3 ) GLOBAL_UNCERTAINTY_ASSIGNED_CONTEXT ( ( #5907 ) ) GLOBAL_UNIT_ASSIGNED_CONTEXT ( ( #19257, #34198, #17793 ) ) REPRESENTATION_CONTEXT ( 'NONE', 'WORKASPACE' ) );
#24287=CIRCLE ( 'NONE', #29451, 1.000000000000000444 ) ;
#24371=CYLINDRICAL_SURFACE ( 'NONE', #22135, 1.000000000000000888 ) ;
#24377=FACE_BOUND ( 'NONE', #28473, .T. ) ;
#24467=EDGE_CURVE ( 'NONE', #26822, #18180, #4748, .T. ) ;
#24700=DIRECTION ( 'NONE',  ( -1.783119874454246424E-31, -1.187911941725854497E-31, 1.000000000000000000 ) ) ;
#24778=VECTOR ( 'NONE', #32454, 1000.000000000000000 ) ;
#24844=ORIENTED_EDGE ( 'NONE', *, *, #17360, .T. ) ;
#24905=DIRECTION ( 'NONE',  ( 1.000000000000000000, 0.000000000000000000, 0.000000000000000000 ) ) ;
#24930=CARTESIAN_POINT ( 'NONE',  ( -0.2142857142857362840, -10.49781318335649161, -1.200000000000006617 ) ) ;
#24931=CARTESIAN_POINT ( 'NONE',  ( 0.2142857142857085284, -10.49781318335649161, 0.000000000000000000 ) ) ;
#24965=CARTESIAN_POINT ( 'NONE',  ( 4.121423858225409909, -12.61643262889541894, -1.200000000000006617 ) ) ;
#25051=VERTEX_POINT ( 'NONE', #35128 ) ;
#25085=DIRECTION ( 'NONE',  ( 1.783119874454246424E-31, 1.187911941725854497E-31, -1.000000000000000000 ) ) ;
#25135=AXIS2_PLACEMENT_3D ( 'NONE', #1028, #11632, #27691 ) ;
#25164=EDGE_LOOP ( 'NONE', ( #21508, #18416, #10196, #10652 ) ) ;
#25186=LINE ( 'NONE', #25535, #14408 ) ;
#25189=FACE_OUTER_BOUND ( 'NONE', #14861, .T. ) ;
#25214=EDGE_LOOP ( 'NONE', ( #21871, #14676, #8887, #19733, #382, #29507, #32158, #16330, #35439, #18210, #22575, #18281, #23980, #17561, #17837, #14945 ) ) ;
#25221=VERTEX_POINT ( 'NONE', #22296 ) ;
#25249=SURFACE_STYLE_USAGE ( .BOTH. , #13741 ) ;
#25254=VECTOR ( 'NONE', #19687, 1000.000000000000000 ) ;
#25363=DIRECTION ( 'NONE',  ( 1.691777834109591064E-31, -1.187911941725854715E-31, 1.000000000000000000 ) ) ;
#25376=ORIENTED_EDGE ( 'NONE', *, *, #22975, .T. ) ;
#25453=UNCERTAINTY_MEASURE_WITH_UNIT (LENGTH_MEASURE( 1.000000000000000082E-05 ), #11202, 'distance_accuracy_value', 'NONE');
#25530=ORIENTED_EDGE ( 'NONE', *, *, #26046, .T. ) ;
#25535=CARTESIAN_POINT ( 'NONE',  ( 0.2142857142857085284, -10.49781318335649161, -1.200000000000006617 ) ) ;
#25541=FACE_OUTER_BOUND ( 'NONE', #25214, .T. ) ;
#25570=SURFACE_STYLE_USAGE ( .BOTH. , #28266 ) ;
#25571=CIRCLE ( 'NONE', #27297, 14.70000000000000107 ) ;
#25612=ADVANCED_FACE ( 'NONE', ( #19537 ), #22250, .T. ) ;
#25642=DIRECTION ( 'NONE',  ( 1.783119874454246424E-31, 1.187911941725854497E-31, -1.000000000000000000 ) ) ;
#25659=VERTEX_POINT ( 'NONE', #29849 ) ;
#25889=EDGE_LOOP ( 'NONE', ( #9785, #12677, #22144, #10026 ) ) ;
#25894=CARTESIAN_POINT ( 'NONE',  ( -1.600000000000004086, -12.74999999999999822, -1.200000000000006617 ) ) ;
#25966=CARTESIAN_POINT ( 'NONE',  ( -0.2142857142857362840, -10.49781318335649161, -1.200000000000006617 ) ) ;
#25980=CIRCLE ( 'NONE', #34023, 1.000000000000000444 ) ;
#26030=CARTESIAN_POINT ( 'NONE',  ( 0.2142857142857085284, -10.49781318335649161, -1.200000000000006617 ) ) ;
#26043=ORIENTED_EDGE ( 'NONE', *, *, #24467, .T. ) ;
#26046=EDGE_CURVE ( 'NONE', #19601, #13102, #8451, .T. ) ;
#26048=ORIENTED_EDGE ( 'NONE', *, *, #17774, .T. ) ;
#26119=ORIENTED_EDGE ( 'NONE', *, *, #17774, .F. ) ;
#26145=DIRECTION ( 'NONE',  ( 1.783119874454246424E-31, 1.187911941725854497E-31, -1.000000000000000000 ) ) ;
#26180=EDGE_CURVE ( 'NONE', #29210, #31461, #35213, .T. ) ;
#26305=EDGE_CURVE ( 'NONE', #15074, #25051, #11587, .T. ) ;
#26439=ORIENTED_EDGE ( 'NONE', *, *, #1833, .T. ) ;
#26449=ORIENTED_EDGE ( 'NONE', *, *, #30915, .T. ) ;
#26457=DIRECTION ( 'NONE',  ( -1.783119874454246424E-31, -1.187911941725854497E-31, 1.000000000000000000 ) ) ;
#26477=AXIS2_PLACEMENT_3D ( 'NONE', #12545, #20431, #4636 ) ;
#26505=DIRECTION ( 'NONE',  ( 1.000000000000000000, 0.000000000000000000, 0.000000000000000000 ) ) ;
#26546=FACE_OUTER_BOUND ( 'NONE', #9019, .T. ) ;
#26577=VECTOR ( 'NONE', #13277, 1000.000000000000114 ) ;
#26581=DIRECTION ( 'NONE',  ( -1.783119874454246424E-31, -1.187911941725854497E-31, 1.000000000000000000 ) ) ;
#26589=CARTESIAN_POINT ( 'NONE',  ( 0.000000000000000000, 0.000000000000000000, 0.000000000000000000 ) ) ;
#26598=CARTESIAN_POINT ( 'NONE',  ( 0.000000000000000000, 0.000000000000000000, 0.000000000000000000 ) ) ;
#26605=FACE_OUTER_BOUND ( 'NONE', #29283, .T. ) ;
#26614=VECTOR ( 'NONE', #4386, 1000.000000000000000 ) ;
#26638=EDGE_CURVE ( 'NONE', #31912, #14640, #20940, .T. ) ;
#26689=DIRECTION ( 'NONE',  ( -1.783119874454246424E-31, -1.187911941725854497E-31, 1.000000000000000000 ) ) ;
#26691=ORIENTED_EDGE ( 'NONE', *, *, #30376, .T. ) ;
#26696=CARTESIAN_POINT ( 'NONE',  ( 0.000000000000000000, 0.000000000000000000, -1.200000000000006617 ) ) ;
#26699=CARTESIAN_POINT ( 'NONE',  ( -3.413765605486555721, -14.29811891091961584, -1.200000000000006617 ) ) ;
#26720=ORIENTED_EDGE ( 'NONE', *, *, #30376, .F. ) ;
#26753=CARTESIAN_POINT ( 'NONE',  ( 0.2142857142857085284, -10.49781318335649161, 0.000000000000000000 ) ) ;
#26788=DIRECTION ( 'NONE',  ( 1.000000000000000000, 0.000000000000000000, 0.000000000000000000 ) ) ;
#26822=VERTEX_POINT ( 'NONE', #9152 ) ;
#26846=COLOUR_RGB ( '', 0.72549020, 0.75294118, 0.79215686) ;
#26894=EDGE_CURVE ( 'NONE', #33119, #29210, #25571, .T. ) ;
#26899=AXIS2_PLACEMENT_3D ( 'NONE', #21157, #26581, #18633 ) ;
#26964=LINE ( 'NONE', #2306, #26577 ) ;
#27067=CARTESIAN_POINT ( 'NONE',  ( -4.121423858225413461, -12.61643262889540473, -1.200000000000006617 ) ) ;
#27082=ORIENTED_EDGE ( 'NONE', *, *, #6170, .F. ) ;
#27133=CARTESIAN_POINT ( 'NONE',  ( 5.639656061357293915, -10.48075544252193048, 0.000000000000000000 ) ) ;
#27223=DIRECTION ( 'NONE',  ( -1.783119874454246424E-31, -1.187911941725854497E-31, 1.000000000000000000 ) ) ;
#27246=EDGE_CURVE ( 'NONE', #23706, #7811, #15794, .T. ) ;
#27261=FACE_OUTER_BOUND ( 'NONE', #9198, .T. ) ;
#27297=AXIS2_PLACEMENT_3D ( 'NONE', #20116, #34370, #3590 ) ;
#27338=DIRECTION ( 'NONE',  ( -1.783119874454246424E-31, -1.187911941725854497E-31, 1.000000000000000000 ) ) ;
#27345=ORIENTED_EDGE ( 'NONE', *, *, #24020, .T. ) ;
#27431=SURFACE_STYLE_FILL_AREA ( #33176 ) ;
#27505=DIRECTION ( 'NONE',  ( -1.783119874454246424E-31, -1.187911941725854497E-31, 1.000000000000000000 ) ) ;
#27510=ORIENTED_EDGE ( 'NONE', *, *, #11507, .F. ) ;
#27561=PRODUCT_DEFINITION ( 'UNKNOWN', '', #1152, #21541 ) ;
#27583=AXIS2_PLACEMENT_3D ( 'NONE', #26696, #5087, #21972 ) ;
#27605=LINE ( 'NONE', #21818, #24778 ) ;
#27621=EDGE_LOOP ( 'NONE', ( #27510, #23918, #15251, #32971 ) ) ;
#27633=VECTOR ( 'NONE', #5914, 1000.000000000000000 ) ;
#27654=ORIENTED_EDGE ( 'NONE', *, *, #17897, .T. ) ;
#27660=AXIS2_PLACEMENT_3D ( 'NONE', #27674, #27505, #32525 ) ;
#27663=VECTOR ( 'NONE', #8136, 1000.000000000000114 ) ;
#27674=CARTESIAN_POINT ( 'NONE',  ( -6.938893903907228378E-15, 0.7408941433508786645, 0.000000000000000000 ) ) ;
#27691=DIRECTION ( 'NONE',  ( 1.000000000000000000, 0.000000000000000000, 0.000000000000000000 ) ) ;
#27695=EDGE_LOOP ( 'NONE', ( #32172, #13915, #539, #20703 ) ) ;
#27728=ORIENTED_EDGE ( 'NONE', *, *, #31287, .T. ) ;
#27753=CYLINDRICAL_SURFACE ( 'NONE', #2473, 1.000000000000000888 ) ;
#27847=AXIS2_PLACEMENT_3D ( 'NONE', #30146, #5483, #13763 ) ;
#27917=VECTOR ( 'NONE', #10714, 1000.000000000000114 ) ;
#28106=FACE_OUTER_BOUND ( 'NONE', #27695, .T. ) ;
#28184=AXIS2_PLACEMENT_3D ( 'NONE', #26598, #1936, #23896 ) ;
#28212=VERTEX_POINT ( 'NONE', #34182 ) ;
#28241=CARTESIAN_POINT ( 'NONE',  ( 3.983177536951269193, -13.66651769228263724, -1.200000000000006617 ) ) ;
#28266=SURFACE_SIDE_STYLE ('',( #34560 ) ) ;
#28335=CARTESIAN_POINT ( 'NONE',  ( 0.000000000000000000, 0.000000000000000000, -1.200000000000006617 ) ) ;
#28473=EDGE_LOOP ( 'NONE', ( #33438, #34018 ) ) ;
#28513=DIRECTION ( 'NONE',  ( 0.9914448613738107152, -0.1305261922200497138, -2.588645552990029003E-31 ) ) ;
#28514=CIRCLE ( 'NONE', #13561, 10.50000000000000178 ) ;
#28592=DIRECTION ( 'NONE',  ( 0.02040816326530624225, 0.9997917317482359900, -1.513872302910508719E-31 ) ) ;
#28786=PRODUCT ( 'circlip for shafts normal_din_Circlip DIN 471 - 22 x 1.2', 'circlip for shafts normal_din_Circlip DIN 471 - 22 x 1.2', '', ( #11306 ) ) ;
#28792=DIRECTION ( 'NONE',  ( 1.000000000000000000, 0.000000000000000000, -1.691777834109591283E-31 ) ) ;
#28795=( NAMED_UNIT ( * ) PLANE_ANGLE_UNIT ( ) SI_UNIT ( $, .RADIAN. ) );
#28862=DIRECTION ( 'NONE',  ( -1.783119874454246424E-31, -1.187911941725854497E-31, 1.000000000000000000 ) ) ;
#28915=LINE ( 'NONE', #3722, #29681 ) ;
#28969=ADVANCED_FACE ( 'NONE', ( #23504 ), #4794, .F. ) ;
#29038=LINE ( 'NONE', #1865, #26614 ) ;
#29049=VERTEX_POINT ( 'NONE', #33212 ) ;
#29210=VERTEX_POINT ( 'NONE', #30857 ) ;
#29283=EDGE_LOOP ( 'NONE', ( #11296, #22696, #2050, #12796 ) ) ;
#29304=CARTESIAN_POINT ( 'NONE',  ( 6.896599878636562764, -12.98179148322720167, -1.200000000000006617 ) ) ;
#29311=ADVANCED_FACE ( 'NONE', ( #2015 ), #18378, .T. ) ;
#29357=CIRCLE ( 'NONE', #26477, 10.50000000000000178 ) ;
#29379=CARTESIAN_POINT ( 'NONE',  ( -6.938893903907228378E-15, 0.7408941433508786645, -1.200000000000006617 ) ) ;
#29405=CIRCLE ( 'NONE', #1832, 1.000000000000000888 ) ;
#29448=LINE ( 'NONE', #26753, #27917 ) ;
#29451=AXIS2_PLACEMENT_3D ( 'NONE', #23708, #9486, #34700 ) ;
#29507=ORIENTED_EDGE ( 'NONE', *, *, #16313, .F. ) ;
#29562=EDGE_CURVE ( 'NONE', #14640, #18916, #29791, .T. ) ;
#29603=LINE ( 'NONE', #4942, #29637 ) ;
#29637=VECTOR ( 'NONE', #16418, 1000.000000000000000 ) ;
#29656=CARTESIAN_POINT ( 'NONE',  ( 1.600000000000004086, -12.74999999999999822, 0.000000000000000000 ) ) ;
#29681=VECTOR ( 'NONE', #23323, 1000.000000000000000 ) ;
#29791=CIRCLE ( 'NONE', #2206, 14.70000000000000107 ) ;
#29828=AXIS2_PLACEMENT_3D ( 'NONE', #1922, #15392, #6584 ) ;
#29848=DIRECTION ( 'NONE',  ( -1.783119874454246424E-31, -1.187911941725854497E-31, 1.000000000000000000 ) ) ;
#29849=CARTESIAN_POINT ( 'NONE',  ( 4.121423858225409909, -12.61643262889541894, 0.000000000000000000 ) ) ;
#29867=FACE_OUTER_BOUND ( 'NONE', #16761, .T. ) ;
#29963=FACE_BOUND ( 'NONE', #1827, .T. ) ;
#29973=MECHANICAL_DESIGN_GEOMETRIC_PRESENTATION_REPRESENTATION('',(#20740),#22468);
#29991=EDGE_CURVE ( 'NONE', #19897, #10552, #135, .T. ) ;
#30047=CARTESIAN_POINT ( 'NONE',  ( -6.938893903907228378E-15, 0.7408941433508786645, 0.000000000000000000 ) ) ;
#30079=AXIS2_PLACEMENT_3D ( 'NONE', #17867, #28862, #34996 ) ;
#30146=CARTESIAN_POINT ( 'NONE',  ( 0.000000000000000000, 0.000000000000000000, 0.000000000000000000 ) ) ;
#30252=CARTESIAN_POINT ( 'NONE',  ( -4.121423858225413461, -12.61643262889540473, -1.200000000000006617 ) ) ;
#30285=SHAPE_REPRESENTATION ( 'circlip for shafts normal_din_Circlip DIN 471 - 22 x 1.2', ( #21307 ), #24211 ) ;
#30346=CARTESIAN_POINT ( 'NONE',  ( 12.55910585664917711, 0.7408941433508786645, -1.200000000000006617 ) ) ;
#30376=EDGE_CURVE ( 'NONE', #9296, #15714, #29603, .T. ) ;
#30406=ADVANCED_FACE ( 'NONE', ( #24028 ), #24371, .F. ) ;
#30542=CARTESIAN_POINT ( 'NONE',  ( -6.938893903907228378E-15, 0.7408941433508786645, -1.200000000000006617 ) ) ;
#30570=CIRCLE ( 'NONE', #19076, 2.799122904894268071 ) ;
#30577=PLANE ( 'NONE',  #4822 ) ;
#30582=LINE ( 'NONE', #13499, #27633 ) ;
#30624=EDGE_CURVE ( 'NONE', #31461, #11231, #15133, .T. ) ;
#30667=CARTESIAN_POINT ( 'NONE',  ( 6.896599878636562764, -12.98179148322720167, -1.200000000000006617 ) ) ;
#30672=DIRECTION ( 'NONE',  ( 1.000000000000000000, 0.000000000000000000, 0.000000000000000000 ) ) ;
#30684=DIRECTION ( 'NONE',  ( -1.783119874454246424E-31, -1.187911941725854497E-31, 1.000000000000000000 ) ) ;
#30758=VECTOR ( 'NONE', #7240, 1000.000000000000000 ) ;
#30857=CARTESIAN_POINT ( 'NONE',  ( -0.3000000000000016542, -14.69693845669907439, -1.200000000000006617 ) ) ;
#30915=EDGE_CURVE ( 'NONE', #19601, #25221, #7409, .T. ) ;
#30922=AXIS2_PLACEMENT_3D ( 'NONE', #14931, #20323, #17636 ) ;
#30960=PRESENTATION_STYLE_ASSIGNMENT (( #25570 ) ) ;
#31037=CARTESIAN_POINT ( 'NONE',  ( 4.121423858225409909, -12.61643262889541894, -1.200000000000006617 ) ) ;
#31203=EDGE_LOOP ( 'NONE', ( #2368, #22870, #33528, #22518 ) ) ;
#31279=DIRECTION ( 'NONE',  ( 1.000000000000000000, 0.000000000000000000, 0.000000000000000000 ) ) ;
#31287=EDGE_CURVE ( 'NONE', #25221, #580, #7544, .T. ) ;
#31304=DIRECTION ( 'NONE',  ( -1.783119874454246424E-31, -1.187911941725854497E-31, 1.000000000000000000 ) ) ;
#31313=FILL_AREA_STYLE ('',( #6467 ) ) ;
#31341=ORIENTED_EDGE ( 'NONE', *, *, #34208, .T. ) ;
#31400=CIRCLE ( 'NONE', #17012, 12.55910585664918422 ) ;
#31428=DIRECTION ( 'NONE',  ( 1.000000000000000000, 0.000000000000000000, 0.000000000000000000 ) ) ;
#31439=EDGE_LOOP ( 'NONE', ( #31341, #26449, #34615, #8504 ) ) ;
#31452=FACE_OUTER_BOUND ( 'NONE', #23694, .T. ) ;
#31461=VERTEX_POINT ( 'NONE', #5730 ) ;
#31749=CARTESIAN_POINT ( 'NONE',  ( 3.239593890920905217, -13.56862304811760822, -1.200000000000006617 ) ) ;
#31818=CARTESIAN_POINT ( 'NONE',  ( -5.639656061357301020, -10.48075544252181857, -1.200000000000006617 ) ) ;
#31836=ORIENTED_EDGE ( 'NONE', *, *, #26638, .T. ) ;
#31840=CARTESIAN_POINT ( 'NONE',  ( -6.938893903907228378E-15, 0.7408941433508786645, -1.200000000000006617 ) ) ;
#31873=VERTEX_POINT ( 'NONE', #27133 ) ;
#31912=VERTEX_POINT ( 'NONE', #1933 ) ;
#32158=ORIENTED_EDGE ( 'NONE', *, *, #26046, .F. ) ;
#32172=ORIENTED_EDGE ( 'NONE', *, *, #10966, .T. ) ;
#32218=CIRCLE ( 'NONE', #21281, 12.55910585664918422 ) ;
#32454=DIRECTION ( 'NONE',  ( -1.783119874454246424E-31, -1.187911941725854497E-31, 1.000000000000000000 ) ) ;
#32506=ORIENTED_EDGE ( 'NONE', *, *, #23305, .T. ) ;
#32525=DIRECTION ( 'NONE',  ( 1.000000000000000000, 0.000000000000000000, -1.691777834109591064E-31 ) ) ;
#32595=AXIS2_PLACEMENT_3D ( 'NONE', #7153, #2138, #26788 ) ;
#32648=ORIENTED_EDGE ( 'NONE', *, *, #12544, .T. ) ;
#32653=CARTESIAN_POINT ( 'NONE',  ( 1.600000000000004086, -12.74999999999999822, -1.200000000000006617 ) ) ;
#32660=PLANE ( 'NONE',  #34447 ) ;
#32693=CARTESIAN_POINT ( 'NONE',  ( -3.413765605486555721, -14.29811891091961584, -1.200000000000006617 ) ) ;
#32862=FACE_OUTER_BOUND ( 'NONE', #4799, .T. ) ;
#32882=CARTESIAN_POINT ( 'NONE',  ( -10.50000000000000178, 1.285879139104719253E-15, -1.200000000000006617 ) ) ;
#32942=ORIENTED_EDGE ( 'NONE', *, *, #34621, .T. ) ;
#32959=VECTOR ( 'NONE', #9275, 1000.000000000000000 ) ;
#32971=ORIENTED_EDGE ( 'NONE', *, *, #10564, .F. ) ;
#32975=DIRECTION ( 'NONE',  ( 1.000000000000000000, 0.000000000000000000, 0.000000000000000000 ) ) ;
#33119=VERTEX_POINT ( 'NONE', #32693 ) ;
#33153=DIRECTION ( 'NONE',  ( 1.000000000000000000, 0.000000000000000000, 0.000000000000000000 ) ) ;
#33176=FILL_AREA_STYLE ('',( #571 ) ) ;
#33182=VECTOR ( 'NONE', #10533, 1000.000000000000000 ) ;
#33212=CARTESIAN_POINT ( 'NONE',  ( -10.50000000000000178, 1.285879139104719253E-15, -8.088905766426390583E-30 ) ) ;
#33256=CARTESIAN_POINT ( 'NONE',  ( 1.600000000000004086, -12.74999999999999822, 0.000000000000000000 ) ) ;
#33438=ORIENTED_EDGE ( 'NONE', *, *, #24181, .F. ) ;
#33467=VERTEX_POINT ( 'NONE', #30252 ) ;
#33471=ORIENTED_EDGE ( 'NONE', *, *, #11890, .T. ) ;
#33514=CARTESIAN_POINT ( 'NONE',  ( 3.413765605486549060, -14.29811891091956078, -1.200000000000006617 ) ) ;
#33528=ORIENTED_EDGE ( 'NONE', *, *, #26894, .T. ) ;
#33729=ORIENTED_EDGE ( 'NONE', *, *, #11259, .F. ) ;
#33739=EDGE_CURVE ( 'NONE', #15714, #2729, #3923, .T. ) ;
#33755=VECTOR ( 'NONE', #2798, 1000.000000000000000 ) ;
#33923=CARTESIAN_POINT ( 'NONE',  ( -6.938893903907228378E-15, 0.7408941433508786645, 0.000000000000000000 ) ) ;
#33981=CYLINDRICAL_SURFACE ( 'NONE', #34392, 10.50000000000000178 ) ;
#34018=ORIENTED_EDGE ( 'NONE', *, *, #27246, .F. ) ;
#34023=AXIS2_PLACEMENT_3D ( 'NONE', #9132, #27223, #18919 ) ;
#34099=DIRECTION ( 'NONE',  ( 0.1305261922200497138, 0.9914448613738107152, -1.707538432756455455E-31 ) ) ;
#34167=EDGE_CURVE ( 'NONE', #8141, #4040, #18802, .T. ) ;
#34182=CARTESIAN_POINT ( 'NONE',  ( 3.983177536951269193, -13.66651769228263724, 0.000000000000000000 ) ) ;
#34195=DIRECTION ( 'NONE',  ( -1.783119874454246424E-31, -1.187911941725854497E-31, 1.000000000000000000 ) ) ;
#34198=( NAMED_UNIT ( * ) PLANE_ANGLE_UNIT ( ) SI_UNIT ( $, .RADIAN. ) );
#34208=EDGE_CURVE ( 'NONE', #14643, #19601, #9684, .T. ) ;
#34244=ORIENTED_EDGE ( 'NONE', *, *, #12053, .T. ) ;
#34265=FACE_OUTER_BOUND ( 'NONE', #13897, .T. ) ;
#34370=DIRECTION ( 'NONE',  ( -1.783119874454246424E-31, -1.187911941725854497E-31, 1.000000000000000000 ) ) ;
#34392=AXIS2_PLACEMENT_3D ( 'NONE', #6071, #23162, #6250 ) ;
#34447=AXIS2_PLACEMENT_3D ( 'NONE', #13048, #5471, #24202 ) ;
#34472=ORIENTED_EDGE ( 'NONE', *, *, #26305, .T. ) ;
#34521=ORIENTED_EDGE ( 'NONE', *, *, #21065, .F. ) ;
#34536=CIRCLE ( 'NONE', #27660, 12.55910585664918422 ) ;
#34553=ORIENTED_EDGE ( 'NONE', *, *, #23305, .F. ) ;
#34560=SURFACE_STYLE_FILL_AREA ( #31313 ) ;
#34566=DIRECTION ( 'NONE',  ( 1.000000000000000000, 0.000000000000000000, -1.691777834109591283E-31 ) ) ;
#34615=ORIENTED_EDGE ( 'NONE', *, *, #34621, .F. ) ;
#34621=EDGE_CURVE ( 'NONE', #12235, #25221, #31400, .T. ) ;
#34674=DIRECTION ( 'NONE',  ( -1.783119874454246424E-31, -1.187911941725854497E-31, 1.000000000000000000 ) ) ;
#34677=LINE ( 'NONE', #7116, #22978 ) ;
#34683=AXIS2_PLACEMENT_3D ( 'NONE', #7002, #17978, #1433 ) ;
#34700=DIRECTION ( 'NONE',  ( 1.000000000000000000, 0.000000000000000000, 0.000000000000000000 ) ) ;
#34890=CARTESIAN_POINT ( 'NONE',  ( -2.600000000000004530, -12.74999999999999822, -1.200000000000006617 ) ) ;
#34902=VECTOR ( 'NONE', #20460, 1000.000000000000000 ) ;
#34958=MANIFOLD_SOLID_BREP ( 'Body', #10081 ) ;
#34996=DIRECTION ( 'NONE',  ( 1.000000000000000000, 0.000000000000000000, 0.000000000000000000 ) ) ;
#35052=ORIENTED_EDGE ( 'NONE', *, *, #11570, .F. ) ;
#35128=CARTESIAN_POINT ( 'NONE',  ( 3.413765605486549060, -14.29811891091956078, 0.000000000000000000 ) ) ;
#35153=VERTEX_POINT ( 'NONE', #15122 ) ;
#35204=EDGE_CURVE ( 'NONE', #15074, #4315, #13651, .T. ) ;
#35213=LINE ( 'NONE', #24930, #33182 ) ;
#35228=ORIENTED_EDGE ( 'NONE', *, *, #13246, .T. ) ;
#35335=DIRECTION ( 'NONE',  ( -1.783119874454246424E-31, -1.187911941725854497E-31, 1.000000000000000000 ) ) ;
#35439=ORIENTED_EDGE ( 'NONE', *, *, #12848, .F. ) ;
#35475=AXIS2_PLACEMENT_3D ( 'NONE', #30542, #29848, #13975 ) ;
#35544=EDGE_CURVE ( 'NONE', #11231, #29049, #29357, .T. ) ;
ENDSEC;
END-ISO-10303-21;
